ISO-10303-21;
HEADER;
/* Generated by software containing ST-Developer
 * from STEP Tools, Inc. (www.steptools.com) 
 */

FILE_DESCRIPTION(
/* description */ ('Turntable on roller ring'),
/* implementation_level */ '2;1');

FILE_NAME(
/* name */ 'Centre spindle.step',
/* time_stamp */ '2026-10-28T03:23:59-07:00',
/* author */ (''),
/* organization */ (''),
/* preprocessor_version */ 'ST-DEVELOPER v20.2',
/* originating_system */ 'Autodesk Translation Framework v15.17.0.0',
/* authorisation */ '');

FILE_SCHEMA (('AUTOMOTIVE_DESIGN { 1 0 10303 214 3 1 1 }'));
ENDSEC;

DATA;
#10=MECHANICAL_DESIGN_GEOMETRIC_PRESENTATION_REPRESENTATION('',(#637),#16281);
#518=SHAPE_REPRESENTATION_RELATIONSHIP('SRR','None',#16534,#573);
#573=ADVANCED_BREP_SHAPE_REPRESENTATION('',(#708),#16228);
#637=STYLED_ITEM('',(#16946),#708);
#708=MANIFOLD_SOLID_BREP('Body1',#8379);
#833=FACE_BOUND('',#1986,.T.);
#834=FACE_BOUND('',#1990,.T.);
#835=FACE_BOUND('',#1991,.T.);
#836=FACE_BOUND('',#1992,.T.);
#1051=PLANE('',#9393);
#1052=PLANE('',#9397);
#1053=PLANE('',#9401);
#1054=PLANE('',#9402);
#1055=PLANE('',#9409);
#1056=PLANE('',#9410);
#1398=FACE_OUTER_BOUND('',#1979,.T.);
#1399=FACE_OUTER_BOUND('',#1980,.T.);
#1400=FACE_OUTER_BOUND('',#1981,.T.);
#1401=FACE_OUTER_BOUND('',#1982,.T.);
#1402=FACE_OUTER_BOUND('',#1983,.T.);
#1403=FACE_OUTER_BOUND('',#1984,.T.);
#1404=FACE_OUTER_BOUND('',#1985,.T.);
#1405=FACE_OUTER_BOUND('',#1987,.T.);
#1406=FACE_OUTER_BOUND('',#1988,.T.);
#1407=FACE_OUTER_BOUND('',#1989,.T.);
#1408=FACE_OUTER_BOUND('',#1993,.T.);
#1979=EDGE_LOOP('',(#6293,#6294,#6295,#6296));
#1980=EDGE_LOOP('',(#6297));
#1981=EDGE_LOOP('',(#6298,#6299,#6300,#6301));
#1982=EDGE_LOOP('',(#6302));
#1983=EDGE_LOOP('',(#6303,#6304,#6305,#6306));
#1984=EDGE_LOOP('',(#6307));
#1985=EDGE_LOOP('',(#6308));
#1986=EDGE_LOOP('',(#6309));
#1987=EDGE_LOOP('',(#6310,#6311,#6312,#6313));
#1988=EDGE_LOOP('',(#6314,#6315,#6316,#6317));
#1989=EDGE_LOOP('',(#6318));
#1990=EDGE_LOOP('',(#6319));
#1991=EDGE_LOOP('',(#6320));
#1992=EDGE_LOOP('',(#6321));
#1993=EDGE_LOOP('',(#6322));
#2618=LINE('',#14098,#3101);
#2619=LINE('',#14105,#3102);
#2620=LINE('',#14112,#3103);
#2621=LINE('',#14123,#3104);
#2622=LINE('',#14126,#3105);
#3101=VECTOR('',#11029,0.165);
#3102=VECTOR('',#11038,0.165);
#3103=VECTOR('',#11047,0.165);
#3104=VECTOR('',#11062,1.75);
#3105=VECTOR('',#11065,1.25);
#3640=CIRCLE('',#9391,0.165);
#3641=CIRCLE('',#9392,0.165);
#3642=CIRCLE('',#9395,0.165);
#3643=CIRCLE('',#9396,0.165);
#3644=CIRCLE('',#9399,0.165);
#3645=CIRCLE('',#9400,0.165);
#3646=CIRCLE('',#9403,1.75);
#3647=CIRCLE('',#9404,1.25);
#3648=CIRCLE('',#9406,1.75);
#3649=CIRCLE('',#9408,1.25);
#4169=VERTEX_POINT('',#14095);
#4170=VERTEX_POINT('',#14097);
#4171=VERTEX_POINT('',#14102);
#4172=VERTEX_POINT('',#14104);
#4173=VERTEX_POINT('',#14109);
#4174=VERTEX_POINT('',#14111);
#4175=VERTEX_POINT('',#14116);
#4176=VERTEX_POINT('',#14118);
#4177=VERTEX_POINT('',#14121);
#4178=VERTEX_POINT('',#14125);
#4957=EDGE_CURVE('',#4169,#4169,#3640,.T.);
#4958=EDGE_CURVE('',#4169,#4170,#2618,.T.);
#4959=EDGE_CURVE('',#4170,#4170,#3641,.T.);
#4960=EDGE_CURVE('',#4171,#4171,#3642,.T.);
#4961=EDGE_CURVE('',#4171,#4172,#2619,.T.);
#4962=EDGE_CURVE('',#4172,#4172,#3643,.T.);
#4963=EDGE_CURVE('',#4173,#4173,#3644,.T.);
#4964=EDGE_CURVE('',#4173,#4174,#2620,.T.);
#4965=EDGE_CURVE('',#4174,#4174,#3645,.T.);
#4966=EDGE_CURVE('',#4175,#4175,#3646,.T.);
#4967=EDGE_CURVE('',#4176,#4176,#3647,.T.);
#4968=EDGE_CURVE('',#4177,#4177,#3648,.T.);
#4969=EDGE_CURVE('',#4177,#4175,#2621,.T.);
#4970=EDGE_CURVE('',#4176,#4178,#2622,.T.);
#4971=EDGE_CURVE('',#4178,#4178,#3649,.T.);
#6293=ORIENTED_EDGE('',*,*,#4957,.F.);
#6294=ORIENTED_EDGE('',*,*,#4958,.T.);
#6295=ORIENTED_EDGE('',*,*,#4959,.F.);
#6296=ORIENTED_EDGE('',*,*,#4958,.F.);
#6297=ORIENTED_EDGE('',*,*,#4957,.T.);
#6298=ORIENTED_EDGE('',*,*,#4960,.F.);
#6299=ORIENTED_EDGE('',*,*,#4961,.T.);
#6300=ORIENTED_EDGE('',*,*,#4962,.F.);
#6301=ORIENTED_EDGE('',*,*,#4961,.F.);
#6302=ORIENTED_EDGE('',*,*,#4960,.T.);
#6303=ORIENTED_EDGE('',*,*,#4963,.F.);
#6304=ORIENTED_EDGE('',*,*,#4964,.T.);
#6305=ORIENTED_EDGE('',*,*,#4965,.F.);
#6306=ORIENTED_EDGE('',*,*,#4964,.F.);
#6307=ORIENTED_EDGE('',*,*,#4963,.T.);
#6308=ORIENTED_EDGE('',*,*,#4966,.F.);
#6309=ORIENTED_EDGE('',*,*,#4967,.F.);
#6310=ORIENTED_EDGE('',*,*,#4968,.F.);
#6311=ORIENTED_EDGE('',*,*,#4969,.T.);
#6312=ORIENTED_EDGE('',*,*,#4966,.T.);
#6313=ORIENTED_EDGE('',*,*,#4969,.F.);
#6314=ORIENTED_EDGE('',*,*,#4967,.T.);
#6315=ORIENTED_EDGE('',*,*,#4970,.T.);
#6316=ORIENTED_EDGE('',*,*,#4971,.T.);
#6317=ORIENTED_EDGE('',*,*,#4970,.F.);
#6318=ORIENTED_EDGE('',*,*,#4968,.T.);
#6319=ORIENTED_EDGE('',*,*,#4959,.T.);
#6320=ORIENTED_EDGE('',*,*,#4962,.T.);
#6321=ORIENTED_EDGE('',*,*,#4965,.T.);
#6322=ORIENTED_EDGE('',*,*,#4971,.F.);
#7729=CYLINDRICAL_SURFACE('',#9390,0.165);
#7730=CYLINDRICAL_SURFACE('',#9394,0.165);
#7731=CYLINDRICAL_SURFACE('',#9398,0.165);
#7732=CYLINDRICAL_SURFACE('',#9405,1.75);
#7733=CYLINDRICAL_SURFACE('',#9407,1.25);
#8001=ADVANCED_FACE('',(#1398),#7729,.F.);
#8002=ADVANCED_FACE('',(#1399),#1051,.T.);
#8003=ADVANCED_FACE('',(#1400),#7730,.F.);
#8004=ADVANCED_FACE('',(#1401),#1052,.T.);
#8005=ADVANCED_FACE('',(#1402),#7731,.F.);
#8006=ADVANCED_FACE('',(#1403),#1053,.T.);
#8007=ADVANCED_FACE('',(#1404,#833),#1054,.F.);
#8008=ADVANCED_FACE('',(#1405),#7732,.T.);
#8009=ADVANCED_FACE('',(#1406),#7733,.T.);
#8010=ADVANCED_FACE('',(#1407,#834,#835,#836),#1055,.T.);
#8011=ADVANCED_FACE('',(#1408),#1056,.F.);
#8379=CLOSED_SHELL('',(#8001,#8002,#8003,#8004,#8005,#8006,#8007,#8008,
#8009,#8010,#8011));
#9389=AXIS2_PLACEMENT_3D('',#14093,#11023,#11024);
#9390=AXIS2_PLACEMENT_3D('',#14094,#11025,#11026);
#9391=AXIS2_PLACEMENT_3D('',#14096,#11027,#11028);
#9392=AXIS2_PLACEMENT_3D('',#14099,#11030,#11031);
#9393=AXIS2_PLACEMENT_3D('',#14100,#11032,#11033);
#9394=AXIS2_PLACEMENT_3D('',#14101,#11034,#11035);
#9395=AXIS2_PLACEMENT_3D('',#14103,#11036,#11037);
#9396=AXIS2_PLACEMENT_3D('',#14106,#11039,#11040);
#9397=AXIS2_PLACEMENT_3D('',#14107,#11041,#11042);
#9398=AXIS2_PLACEMENT_3D('',#14108,#11043,#11044);
#9399=AXIS2_PLACEMENT_3D('',#14110,#11045,#11046);
#9400=AXIS2_PLACEMENT_3D('',#14113,#11048,#11049);
#9401=AXIS2_PLACEMENT_3D('',#14114,#11050,#11051);
#9402=AXIS2_PLACEMENT_3D('',#14115,#11052,#11053);
#9403=AXIS2_PLACEMENT_3D('',#14117,#11054,#11055);
#9404=AXIS2_PLACEMENT_3D('',#14119,#11056,#11057);
#9405=AXIS2_PLACEMENT_3D('',#14120,#11058,#11059);
#9406=AXIS2_PLACEMENT_3D('',#14122,#11060,#11061);
#9407=AXIS2_PLACEMENT_3D('',#14124,#11063,#11064);
#9408=AXIS2_PLACEMENT_3D('',#14127,#11066,#11067);
#9409=AXIS2_PLACEMENT_3D('',#14128,#11068,#11069);
#9410=AXIS2_PLACEMENT_3D('',#14129,#11070,#11071);
#11023=DIRECTION('axis',(0.,0.,1.));
#11024=DIRECTION('refdir',(1.,0.,0.));
#11025=DIRECTION('center_axis',(0.,0.,1.));
#11026=DIRECTION('ref_axis',(1.,0.,0.));
#11027=DIRECTION('center_axis',(0.,0.,1.));
#11028=DIRECTION('ref_axis',(1.,0.,0.));
#11029=DIRECTION('',(0.,0.,1.));
#11030=DIRECTION('center_axis',(0.,0.,-1.));
#11031=DIRECTION('ref_axis',(1.,0.,0.));
#11032=DIRECTION('center_axis',(0.,0.,1.));
#11033=DIRECTION('ref_axis',(1.,0.,0.));
#11034=DIRECTION('center_axis',(0.,0.,1.));
#11035=DIRECTION('ref_axis',(1.,0.,0.));
#11036=DIRECTION('center_axis',(0.,0.,1.));
#11037=DIRECTION('ref_axis',(1.,0.,0.));
#11038=DIRECTION('',(0.,0.,1.));
#11039=DIRECTION('center_axis',(0.,0.,-1.));
#11040=DIRECTION('ref_axis',(1.,0.,0.));
#11041=DIRECTION('center_axis',(0.,0.,1.));
#11042=DIRECTION('ref_axis',(1.,0.,0.));
#11043=DIRECTION('center_axis',(0.,0.,1.));
#11044=DIRECTION('ref_axis',(1.,0.,0.));
#11045=DIRECTION('center_axis',(0.,0.,1.));
#11046=DIRECTION('ref_axis',(1.,0.,0.));
#11047=DIRECTION('',(0.,0.,1.));
#11048=DIRECTION('center_axis',(0.,0.,-1.));
#11049=DIRECTION('ref_axis',(1.,0.,0.));
#11050=DIRECTION('center_axis',(0.,0.,1.));
#11051=DIRECTION('ref_axis',(1.,0.,0.));
#11052=DIRECTION('center_axis',(0.,0.,1.));
#11053=DIRECTION('ref_axis',(1.,0.,0.));
#11054=DIRECTION('center_axis',(0.,0.,1.));
#11055=DIRECTION('ref_axis',(1.,0.,0.));
#11056=DIRECTION('center_axis',(0.,0.,-1.));
#11057=DIRECTION('ref_axis',(1.,0.,0.));
#11058=DIRECTION('center_axis',(0.,0.,1.));
#11059=DIRECTION('ref_axis',(1.,0.,0.));
#11060=DIRECTION('center_axis',(0.,0.,1.));
#11061=DIRECTION('ref_axis',(1.,0.,0.));
#11062=DIRECTION('',(0.,0.,-1.));
#11063=DIRECTION('center_axis',(0.,0.,1.));
#11064=DIRECTION('ref_axis',(1.,0.,0.));
#11065=DIRECTION('',(0.,0.,-1.));
#11066=DIRECTION('center_axis',(0.,0.,1.));
#11067=DIRECTION('ref_axis',(1.,0.,0.));
#11068=DIRECTION('center_axis',(0.,0.,1.));
#11069=DIRECTION('ref_axis',(1.,0.,0.));
#11070=DIRECTION('center_axis',(0.,0.,1.));
#11071=DIRECTION('ref_axis',(1.,0.,0.));
#14093=CARTESIAN_POINT('',(0.,0.,0.));
#14094=CARTESIAN_POINT('Origin',(1.2,0.,4.3));
#14095=CARTESIAN_POINT('',(1.035,-2.02066721859313E-17,4.3));
#14096=CARTESIAN_POINT('Origin',(1.2,0.,4.3));
#14097=CARTESIAN_POINT('',(1.035,2.02066721859313E-17,5.5));
#14098=CARTESIAN_POINT('',(1.035,-2.02066721859313E-17,4.3));
#14099=CARTESIAN_POINT('Origin',(1.2,0.,5.5));
#14100=CARTESIAN_POINT('Origin',(1.2,0.,4.3));
#14101=CARTESIAN_POINT('Origin',(-0.6,1.03923048454133,4.3));
#14102=CARTESIAN_POINT('',(-0.765,1.03923048454133,4.3));
#14103=CARTESIAN_POINT('Origin',(-0.6,1.03923048454133,4.3));
#14104=CARTESIAN_POINT('',(-0.765,1.03923048454133,5.5));
#14105=CARTESIAN_POINT('',(-0.765,1.03923048454133,4.3));
#14106=CARTESIAN_POINT('Origin',(-0.6,1.03923048454133,5.5));
#14107=CARTESIAN_POINT('Origin',(-0.6,1.03923048454133,4.3));
#14108=CARTESIAN_POINT('Origin',(-0.600000000000001,-1.03923048454133,4.3));
#14109=CARTESIAN_POINT('',(-0.765000000000001,-1.03923048454133,4.3));
#14110=CARTESIAN_POINT('Origin',(-0.600000000000001,-1.03923048454133,4.3));
#14111=CARTESIAN_POINT('',(-0.765000000000001,-1.03923048454133,5.5));
#14112=CARTESIAN_POINT('',(-0.765000000000001,-1.03923048454133,4.3));
#14113=CARTESIAN_POINT('Origin',(-0.600000000000001,-1.03923048454133,5.5));
#14114=CARTESIAN_POINT('Origin',(-0.600000000000001,-1.03923048454133,4.3));
#14115=CARTESIAN_POINT('Origin',(0.,0.,4.25));
#14116=CARTESIAN_POINT('',(-1.75,-2.14313189850787E-16,4.25));
#14117=CARTESIAN_POINT('Origin',(0.,0.,4.25));
#14118=CARTESIAN_POINT('',(-1.25,1.53080849893419E-16,4.25));
#14119=CARTESIAN_POINT('Origin',(0.,0.,4.25));
#14120=CARTESIAN_POINT('Origin',(0.,0.,4.25));
#14121=CARTESIAN_POINT('',(-1.75,-2.14313189850787E-16,5.5));
#14122=CARTESIAN_POINT('Origin',(0.,0.,5.5));
#14123=CARTESIAN_POINT('',(-1.75,-2.14313189850787E-16,4.25));
#14124=CARTESIAN_POINT('Origin',(0.,0.,2.));
#14125=CARTESIAN_POINT('',(-1.25,-1.53080849893419E-16,2.));
#14126=CARTESIAN_POINT('',(-1.25,-1.53080849893419E-16,2.));
#14127=CARTESIAN_POINT('Origin',(0.,0.,2.));
#14128=CARTESIAN_POINT('Origin',(0.,0.,5.5));
#14129=CARTESIAN_POINT('Origin',(0.,0.,2.));
#16159=UNCERTAINTY_MEASURE_WITH_UNIT(LENGTH_MEASURE(0.001),#16282,
'DISTANCE_ACCURACY_VALUE',
'Maximum model space distance between geometric entities at asserted c
onnectivities');
#16212=UNCERTAINTY_MEASURE_WITH_UNIT(LENGTH_MEASURE(0.001),#16282,
'DISTANCE_ACCURACY_VALUE',
'Maximum model space distance between geometric entities at asserted c
onnectivities');
#16228=(
GEOMETRIC_REPRESENTATION_CONTEXT(3)
GLOBAL_UNCERTAINTY_ASSIGNED_CONTEXT((#16159))
GLOBAL_UNIT_ASSIGNED_CONTEXT((#16282,#16284,#16285))
REPRESENTATION_CONTEXT('','3D')
);
#16281=(
GEOMETRIC_REPRESENTATION_CONTEXT(3)
GLOBAL_UNCERTAINTY_ASSIGNED_CONTEXT((#16212))
GLOBAL_UNIT_ASSIGNED_CONTEXT((#16282,#16284,#16285))
REPRESENTATION_CONTEXT('','3D')
);
#16282=(
LENGTH_UNIT()
NAMED_UNIT(*)
SI_UNIT(.CENTI.,.METRE.)
);
#16284=(
NAMED_UNIT(*)
PLANE_ANGLE_UNIT()
SI_UNIT($,.RADIAN.)
);
#16285=(
NAMED_UNIT(*)
SI_UNIT($,.STERADIAN.)
SOLID_ANGLE_UNIT()
);
#16301=SHAPE_DEFINITION_REPRESENTATION(#16374,#16534);
#16374=PRODUCT_DEFINITION_SHAPE('',$,#16603);
#16534=SHAPE_REPRESENTATION('',(#9389),#16228);
#16587=PRODUCT_DEFINITION_CONTEXT('part definition',#16793,'design');
#16603=PRODUCT_DEFINITION('Centre spindle','Centre spindle',#16671,#16587);
#16671=PRODUCT_DEFINITION_FORMATION('',$,#16810);
#16793=APPLICATION_CONTEXT(
'Core Data for Automotive Mechanical Design Process');
#16794=PRODUCT_CONTEXT('part definition',#16793,'mechanical');
#16810=PRODUCT('Centre spindle','Centre spindle','Centre spindle',(#16794));
#16940=COLOUR_RGB('Off White',0.89,0.88,0.83);
#16941=FILL_AREA_STYLE_COLOUR('',#16940);
#16942=FILL_AREA_STYLE('',(#16941));
#16943=SURFACE_STYLE_FILL_AREA(#16942);
#16944=SURFACE_SIDE_STYLE('',(#16943));
#16945=SURFACE_STYLE_USAGE(.BOTH.,#16944);
#16946=PRESENTATION_STYLE_ASSIGNMENT((#16945));
ENDSEC;
END-ISO-10303-21;
